ISO-10303-21;
HEADER;
/* Generated by software containing ST-Developer
 * from STEP Tools, Inc. (www.steptools.com) 
 */

FILE_DESCRIPTION(
/* description */ ('Bin tilter linkage'),
/* implementation_level */ '2;1');

FILE_NAME(
/* name */ 'Guide shaft (1).step',
/* time_stamp */ '2026-10-28T03:26:24-07:00',
/* author */ (''),
/* organization */ (''),
/* preprocessor_version */ 'ST-DEVELOPER v20.2',
/* originating_system */ 'Autodesk Translation Framework v15.17.0.0',
/* authorisation */ '');

FILE_SCHEMA (('AUTOMOTIVE_DESIGN { 1 0 10303 214 3 1 1 }'));
ENDSEC;

DATA;
#10=MECHANICAL_DESIGN_GEOMETRIC_PRESENTATION_REPRESENTATION('',(#890),#23728);
#678=SHAPE_REPRESENTATION_RELATIONSHIP('SRR','None',#24142,#784);
#784=ADVANCED_BREP_SHAPE_REPRESENTATION('',(#1004),#23642);
#890=STYLED_ITEM('',(#24765),#1004);
#1004=MANIFOLD_SOLID_BREP('Body1',#12420);
#1604=PLANE('',#14173);
#1605=PLANE('',#14174);
#2119=FACE_OUTER_BOUND('',#3042,.T.);
#2120=FACE_OUTER_BOUND('',#3043,.T.);
#2121=FACE_OUTER_BOUND('',#3044,.T.);
#3042=EDGE_LOOP('',(#9303,#9304,#9305,#9306));
#3043=EDGE_LOOP('',(#9307));
#3044=EDGE_LOOP('',(#9308));
#4080=LINE('',#20784,#4755);
#4755=VECTOR('',#16697,0.6);
#5433=CIRCLE('',#14171,0.6);
#5434=CIRCLE('',#14172,0.6);
#6267=VERTEX_POINT('',#20781);
#6268=VERTEX_POINT('',#20783);
#7391=EDGE_CURVE('',#6267,#6267,#5433,.T.);
#7392=EDGE_CURVE('',#6267,#6268,#4080,.T.);
#7393=EDGE_CURVE('',#6268,#6268,#5434,.T.);
#9303=ORIENTED_EDGE('',*,*,#7391,.F.);
#9304=ORIENTED_EDGE('',*,*,#7392,.T.);
#9305=ORIENTED_EDGE('',*,*,#7393,.T.);
#9306=ORIENTED_EDGE('',*,*,#7392,.F.);
#9307=ORIENTED_EDGE('',*,*,#7391,.T.);
#9308=ORIENTED_EDGE('',*,*,#7393,.F.);
#11384=CYLINDRICAL_SURFACE('',#14170,0.6);
#11844=ADVANCED_FACE('',(#2119),#11384,.T.);
#11845=ADVANCED_FACE('',(#2120),#1604,.T.);
#11846=ADVANCED_FACE('',(#2121),#1605,.F.);
#12420=CLOSED_SHELL('',(#11844,#11845,#11846));
#14169=AXIS2_PLACEMENT_3D('',#20779,#16691,#16692);
#14170=AXIS2_PLACEMENT_3D('',#20780,#16693,#16694);
#14171=AXIS2_PLACEMENT_3D('',#20782,#16695,#16696);
#14172=AXIS2_PLACEMENT_3D('',#20785,#16698,#16699);
#14173=AXIS2_PLACEMENT_3D('',#20786,#16700,#16701);
#14174=AXIS2_PLACEMENT_3D('',#20787,#16702,#16703);
#16691=DIRECTION('axis',(0.,0.,1.));
#16692=DIRECTION('refdir',(1.,0.,0.));
#16693=DIRECTION('center_axis',(1.,0.,0.));
#16694=DIRECTION('ref_axis',(0.,0.,-1.));
#16695=DIRECTION('center_axis',(1.,0.,0.));
#16696=DIRECTION('ref_axis',(0.,0.,-1.));
#16697=DIRECTION('',(-1.,0.,0.));
#16698=DIRECTION('center_axis',(1.,0.,0.));
#16699=DIRECTION('ref_axis',(0.,0.,-1.));
#16700=DIRECTION('center_axis',(1.,0.,0.));
#16701=DIRECTION('ref_axis',(0.,0.,-1.));
#16702=DIRECTION('center_axis',(1.,0.,0.));
#16703=DIRECTION('ref_axis',(0.,0.,-1.));
#20779=CARTESIAN_POINT('',(0.,0.,0.));
#20780=CARTESIAN_POINT('Origin',(-10.,-2.,8.));
#20781=CARTESIAN_POINT('',(1.,-2.,8.6));
#20782=CARTESIAN_POINT('Origin',(1.,-2.,8.));
#20783=CARTESIAN_POINT('',(-10.,-2.,8.6));
#20784=CARTESIAN_POINT('',(-10.,-2.,8.6));
#20785=CARTESIAN_POINT('Origin',(-10.,-2.,8.));
#20786=CARTESIAN_POINT('Origin',(1.,-2.,8.));
#20787=CARTESIAN_POINT('Origin',(-10.,-2.,8.));
#23525=UNCERTAINTY_MEASURE_WITH_UNIT(LENGTH_MEASURE(0.001),#23729,
'DISTANCE_ACCURACY_VALUE',
'Maximum model space distance between geometric entities at asserted c
onnectivities');
#23611=UNCERTAINTY_MEASURE_WITH_UNIT(LENGTH_MEASURE(0.001),#23729,
'DISTANCE_ACCURACY_VALUE',
'Maximum model space distance between geometric entities at asserted c
onnectivities');
#23642=(
GEOMETRIC_REPRESENTATION_CONTEXT(3)
GLOBAL_UNCERTAINTY_ASSIGNED_CONTEXT((#23525))
GLOBAL_UNIT_ASSIGNED_CONTEXT((#23729,#23731,#23732))
REPRESENTATION_CONTEXT('','3D')
);
#23728=(
GEOMETRIC_REPRESENTATION_CONTEXT(3)
GLOBAL_UNCERTAINTY_ASSIGNED_CONTEXT((#23611))
GLOBAL_UNIT_ASSIGNED_CONTEXT((#23729,#23731,#23732))
REPRESENTATION_CONTEXT('','3D')
);
#23729=(
LENGTH_UNIT()
NAMED_UNIT(*)
SI_UNIT(.CENTI.,.METRE.)
);
#23731=(
NAMED_UNIT(*)
PLANE_ANGLE_UNIT()
SI_UNIT($,.RADIAN.)
);
#23732=(
NAMED_UNIT(*)
SI_UNIT($,.STERADIAN.)
SOLID_ANGLE_UNIT()
);
#23763=SHAPE_DEFINITION_REPRESENTATION(#23879,#24142);
#23879=PRODUCT_DEFINITION_SHAPE('',$,#24259);
#24142=SHAPE_REPRESENTATION('',(#14169),#23642);
#24228=PRODUCT_DEFINITION_CONTEXT('part definition',#24578,'design');
#24259=PRODUCT_DEFINITION('Guide shaft (1)','Guide shaft (1)',#24375,#24228);
#24375=PRODUCT_DEFINITION_FORMATION('',$,#24610);
#24578=APPLICATION_CONTEXT(
'Core Data for Automotive Mechanical Design Process');
#24579=PRODUCT_CONTEXT('part definition',#24578,'mechanical');
#24610=PRODUCT('Guide shaft (1)','Guide shaft (1)','Guide shaft (1)',(#24579));
#24759=COLOUR_RGB('Grey',0.48,0.52,0.57);
#24760=FILL_AREA_STYLE_COLOUR('',#24759);
#24761=FILL_AREA_STYLE('',(#24760));
#24762=SURFACE_STYLE_FILL_AREA(#24761);
#24763=SURFACE_SIDE_STYLE('',(#24762));
#24764=SURFACE_STYLE_USAGE(.BOTH.,#24763);
#24765=PRESENTATION_STYLE_ASSIGNMENT((#24764));
ENDSEC;
END-ISO-10303-21;
